ISO-10303-21;
HEADER;
/* Generated by software containing ST-Developer
 * from STEP Tools, Inc. (www.steptools.com) 
 */

FILE_DESCRIPTION(
/* description */ ('STEP AP214'),
/* implementation_level */ '2;1');

FILE_NAME(
/* name */ 'Coupling Clamp Screw 1.step',
/* time_stamp */ '2026-11-15T14:49:54-08:00',
/* author */ (''),
/* organization */ (''),
/* preprocessor_version */ 'ST-DEVELOPER v20.2',
/* originating_system */ 'Autodesk Translation Framework v15.17.0.0',
/* authorisation */ '');

FILE_SCHEMA (('AUTOMOTIVE_DESIGN { 1 0 10303 214 3 1 1 }'));
ENDSEC;

DATA;
#10=MECHANICAL_DESIGN_GEOMETRIC_PRESENTATION_REPRESENTATION('',(#1117),#66721);
#78=TOROIDAL_SURFACE('',#27963,4.3999999999,0.6);
#551=CONICAL_SURFACE('',#27976,2.693275,0.785398163397448);
#1055=SHAPE_REPRESENTATION_RELATIONSHIP('SRR','None',#66918,#1086);
#1086=ADVANCED_BREP_SHAPE_REPRESENTATION('',(#1152),#66709);
#1117=STYLED_ITEM('',(#67095),#1152);
#1152=MANIFOLD_SOLID_BREP('Body1',#25683);
#1404=FACE_BOUND('',#5004,.T.);
#1405=FACE_BOUND('',#5008,.T.);
#2035=PLANE('',#27958);
#2036=PLANE('',#27966);
#2037=PLANE('',#27967);
#2038=PLANE('',#27968);
#2039=PLANE('',#27969);
#2040=PLANE('',#27970);
#2041=PLANE('',#27971);
#2042=PLANE('',#27972);
#2043=PLANE('',#27973);
#2044=PLANE('',#27974);
#3325=FACE_OUTER_BOUND('',#5003,.T.);
#3326=FACE_OUTER_BOUND('',#5005,.T.);
#3327=FACE_OUTER_BOUND('',#5006,.T.);
#3328=FACE_OUTER_BOUND('',#5007,.T.);
#3329=FACE_OUTER_BOUND('',#5009,.T.);
#3330=FACE_OUTER_BOUND('',#5010,.T.);
#3331=FACE_OUTER_BOUND('',#5011,.T.);
#3332=FACE_OUTER_BOUND('',#5012,.T.);
#3333=FACE_OUTER_BOUND('',#5013,.T.);
#3334=FACE_OUTER_BOUND('',#5014,.T.);
#3335=FACE_OUTER_BOUND('',#5015,.T.);
#3336=FACE_OUTER_BOUND('',#5016,.T.);
#3337=FACE_OUTER_BOUND('',#5017,.T.);
#3338=FACE_OUTER_BOUND('',#5018,.T.);
#5003=EDGE_LOOP('',(#21968));
#5004=EDGE_LOOP('',(#21969));
#5005=EDGE_LOOP('',(#21970,#21971,#21972,#21973));
#5006=EDGE_LOOP('',(#21974,#21975,#21976,#21977));
#5007=EDGE_LOOP('',(#21978));
#5008=EDGE_LOOP('',(#21979,#21980,#21981,#21982,#21983,#21984));
#5009=EDGE_LOOP('',(#21985,#21986,#21987,#21988,#21989,#21990));
#5010=EDGE_LOOP('',(#21991,#21992,#21993,#21994));
#5011=EDGE_LOOP('',(#21995,#21996,#21997,#21998));
#5012=EDGE_LOOP('',(#21999,#22000,#22001,#22002));
#5013=EDGE_LOOP('',(#22003,#22004,#22005,#22006));
#5014=EDGE_LOOP('',(#22007,#22008,#22009,#22010));
#5015=EDGE_LOOP('',(#22011,#22012,#22013,#22014));
#5016=EDGE_LOOP('',(#22015));
#5017=EDGE_LOOP('',(#22016,#22017,#22018,#22019));
#5018=EDGE_LOOP('',(#22020,#22021,#22022,#22023));
#6920=LINE('',#64069,#8909);
#6921=LINE('',#64078,#8910);
#6922=LINE('',#64080,#8911);
#6923=LINE('',#64082,#8912);
#6924=LINE('',#64084,#8913);
#6925=LINE('',#64086,#8914);
#6926=LINE('',#64087,#8915);
#6927=LINE('',#64091,#8916);
#6928=LINE('',#64093,#8917);
#6929=LINE('',#64095,#8918);
#6930=LINE('',#64097,#8919);
#6931=LINE('',#64099,#8920);
#6932=LINE('',#64100,#8921);
#6933=LINE('',#64102,#8922);
#6934=LINE('',#64103,#8923);
#6935=LINE('',#64105,#8924);
#6936=LINE('',#64107,#8925);
#6937=LINE('',#64109,#8926);
#6938=LINE('',#64111,#8927);
#6939=LINE('',#64119,#8928);
#6940=LINE('',#64121,#8929);
#8909=VECTOR('',#34035,5.);
#8910=VECTOR('',#34046,1000.);
#8911=VECTOR('',#34047,1000.);
#8912=VECTOR('',#34048,1000.);
#8913=VECTOR('',#34049,1000.);
#8914=VECTOR('',#34050,1000.);
#8915=VECTOR('',#34051,1000.);
#8916=VECTOR('',#34054,1000.);
#8917=VECTOR('',#34055,1000.);
#8918=VECTOR('',#34056,1000.);
#8919=VECTOR('',#34057,1000.);
#8920=VECTOR('',#34058,1000.);
#8921=VECTOR('',#34059,1000.);
#8922=VECTOR('',#34062,1000.);
#8923=VECTOR('',#34063,1000.);
#8924=VECTOR('',#34066,1000.);
#8925=VECTOR('',#34069,1000.);
#8926=VECTOR('',#34072,1000.);
#8927=VECTOR('',#34075,1000.);
#8928=VECTOR('',#34086,2.693275);
#8929=VECTOR('',#34089,3.);
#10343=CIRCLE('',#27959,5.);
#10344=CIRCLE('',#27960,3.);
#10345=CIRCLE('',#27962,5.);
#10346=CIRCLE('',#27964,0.6);
#10347=CIRCLE('',#27965,4.4);
#10348=CIRCLE('',#27975,2.38655);
#10349=CIRCLE('',#27977,3.);
#12375=VERTEX_POINT('',#64063);
#12376=VERTEX_POINT('',#64065);
#12377=VERTEX_POINT('',#64068);
#12378=VERTEX_POINT('',#64072);
#12379=VERTEX_POINT('',#64076);
#12380=VERTEX_POINT('',#64077);
#12381=VERTEX_POINT('',#64079);
#12382=VERTEX_POINT('',#64081);
#12383=VERTEX_POINT('',#64083);
#12384=VERTEX_POINT('',#64085);
#12385=VERTEX_POINT('',#64089);
#12386=VERTEX_POINT('',#64090);
#12387=VERTEX_POINT('',#64092);
#12388=VERTEX_POINT('',#64094);
#12389=VERTEX_POINT('',#64096);
#12390=VERTEX_POINT('',#64098);
#12391=VERTEX_POINT('',#64114);
#12392=VERTEX_POINT('',#64117);
#15677=EDGE_CURVE('',#12375,#12375,#10343,.T.);
#15678=EDGE_CURVE('',#12376,#12376,#10344,.T.);
#15679=EDGE_CURVE('',#12375,#12377,#6920,.T.);
#15680=EDGE_CURVE('',#12377,#12377,#10345,.T.);
#15681=EDGE_CURVE('',#12377,#12378,#10346,.T.);
#15682=EDGE_CURVE('',#12378,#12378,#10347,.T.);
#15683=EDGE_CURVE('',#12379,#12380,#6921,.T.);
#15684=EDGE_CURVE('',#12380,#12381,#6922,.T.);
#15685=EDGE_CURVE('',#12381,#12382,#6923,.T.);
#15686=EDGE_CURVE('',#12382,#12383,#6924,.T.);
#15687=EDGE_CURVE('',#12383,#12384,#6925,.T.);
#15688=EDGE_CURVE('',#12384,#12379,#6926,.T.);
#15689=EDGE_CURVE('',#12385,#12386,#6927,.T.);
#15690=EDGE_CURVE('',#12386,#12387,#6928,.T.);
#15691=EDGE_CURVE('',#12387,#12388,#6929,.T.);
#15692=EDGE_CURVE('',#12388,#12389,#6930,.T.);
#15693=EDGE_CURVE('',#12389,#12390,#6931,.T.);
#15694=EDGE_CURVE('',#12390,#12385,#6932,.T.);
#15695=EDGE_CURVE('',#12381,#12390,#6933,.T.);
#15696=EDGE_CURVE('',#12380,#12385,#6934,.T.);
#15697=EDGE_CURVE('',#12382,#12389,#6935,.T.);
#15698=EDGE_CURVE('',#12383,#12388,#6936,.T.);
#15699=EDGE_CURVE('',#12384,#12387,#6937,.T.);
#15700=EDGE_CURVE('',#12379,#12386,#6938,.T.);
#15701=EDGE_CURVE('',#12391,#12391,#10348,.T.);
#15702=EDGE_CURVE('',#12392,#12392,#10349,.T.);
#15703=EDGE_CURVE('',#12392,#12391,#6939,.T.);
#15704=EDGE_CURVE('',#12392,#12376,#6940,.T.);
#21968=ORIENTED_EDGE('',*,*,#15677,.T.);
#21969=ORIENTED_EDGE('',*,*,#15678,.T.);
#21970=ORIENTED_EDGE('',*,*,#15677,.F.);
#21971=ORIENTED_EDGE('',*,*,#15679,.T.);
#21972=ORIENTED_EDGE('',*,*,#15680,.T.);
#21973=ORIENTED_EDGE('',*,*,#15679,.F.);
#21974=ORIENTED_EDGE('',*,*,#15680,.F.);
#21975=ORIENTED_EDGE('',*,*,#15681,.T.);
#21976=ORIENTED_EDGE('',*,*,#15682,.T.);
#21977=ORIENTED_EDGE('',*,*,#15681,.F.);
#21978=ORIENTED_EDGE('',*,*,#15682,.F.);
#21979=ORIENTED_EDGE('',*,*,#15683,.T.);
#21980=ORIENTED_EDGE('',*,*,#15684,.T.);
#21981=ORIENTED_EDGE('',*,*,#15685,.T.);
#21982=ORIENTED_EDGE('',*,*,#15686,.T.);
#21983=ORIENTED_EDGE('',*,*,#15687,.T.);
#21984=ORIENTED_EDGE('',*,*,#15688,.T.);
#21985=ORIENTED_EDGE('',*,*,#15689,.T.);
#21986=ORIENTED_EDGE('',*,*,#15690,.T.);
#21987=ORIENTED_EDGE('',*,*,#15691,.T.);
#21988=ORIENTED_EDGE('',*,*,#15692,.T.);
#21989=ORIENTED_EDGE('',*,*,#15693,.T.);
#21990=ORIENTED_EDGE('',*,*,#15694,.T.);
#21991=ORIENTED_EDGE('',*,*,#15694,.F.);
#21992=ORIENTED_EDGE('',*,*,#15695,.F.);
#21993=ORIENTED_EDGE('',*,*,#15684,.F.);
#21994=ORIENTED_EDGE('',*,*,#15696,.T.);
#21995=ORIENTED_EDGE('',*,*,#15693,.F.);
#21996=ORIENTED_EDGE('',*,*,#15697,.F.);
#21997=ORIENTED_EDGE('',*,*,#15685,.F.);
#21998=ORIENTED_EDGE('',*,*,#15695,.T.);
#21999=ORIENTED_EDGE('',*,*,#15692,.F.);
#22000=ORIENTED_EDGE('',*,*,#15698,.F.);
#22001=ORIENTED_EDGE('',*,*,#15686,.F.);
#22002=ORIENTED_EDGE('',*,*,#15697,.T.);
#22003=ORIENTED_EDGE('',*,*,#15691,.F.);
#22004=ORIENTED_EDGE('',*,*,#15699,.F.);
#22005=ORIENTED_EDGE('',*,*,#15687,.F.);
#22006=ORIENTED_EDGE('',*,*,#15698,.T.);
#22007=ORIENTED_EDGE('',*,*,#15690,.F.);
#22008=ORIENTED_EDGE('',*,*,#15700,.F.);
#22009=ORIENTED_EDGE('',*,*,#15688,.F.);
#22010=ORIENTED_EDGE('',*,*,#15699,.T.);
#22011=ORIENTED_EDGE('',*,*,#15689,.F.);
#22012=ORIENTED_EDGE('',*,*,#15696,.F.);
#22013=ORIENTED_EDGE('',*,*,#15683,.F.);
#22014=ORIENTED_EDGE('',*,*,#15700,.T.);
#22015=ORIENTED_EDGE('',*,*,#15701,.T.);
#22016=ORIENTED_EDGE('',*,*,#15702,.T.);
#22017=ORIENTED_EDGE('',*,*,#15703,.T.);
#22018=ORIENTED_EDGE('',*,*,#15701,.F.);
#22019=ORIENTED_EDGE('',*,*,#15703,.F.);
#22020=ORIENTED_EDGE('',*,*,#15702,.F.);
#22021=ORIENTED_EDGE('',*,*,#15704,.T.);
#22022=ORIENTED_EDGE('',*,*,#15678,.F.);
#22023=ORIENTED_EDGE('',*,*,#15704,.F.);
#24105=CYLINDRICAL_SURFACE('',#27961,5.);
#24106=CYLINDRICAL_SURFACE('',#27978,3.);
#25278=ADVANCED_FACE('',(#3325,#1404),#2035,.T.);
#25279=ADVANCED_FACE('',(#3326),#24105,.T.);
#25280=ADVANCED_FACE('',(#3327),#78,.T.);
#25281=ADVANCED_FACE('',(#3328,#1405),#2036,.T.);
#25282=ADVANCED_FACE('',(#3329),#2037,.F.);
#25283=ADVANCED_FACE('',(#3330),#2038,.F.);
#25284=ADVANCED_FACE('',(#3331),#2039,.F.);
#25285=ADVANCED_FACE('',(#3332),#2040,.F.);
#25286=ADVANCED_FACE('',(#3333),#2041,.F.);
#25287=ADVANCED_FACE('',(#3334),#2042,.F.);
#25288=ADVANCED_FACE('',(#3335),#2043,.F.);
#25289=ADVANCED_FACE('',(#3336),#2044,.T.);
#25290=ADVANCED_FACE('',(#3337),#551,.T.);
#25291=ADVANCED_FACE('',(#3338),#24106,.T.);
#25683=CLOSED_SHELL('',(#25278,#25279,#25280,#25281,#25282,#25283,#25284,
#25285,#25286,#25287,#25288,#25289,#25290,#25291));
#27957=AXIS2_PLACEMENT_3D('',#64061,#34025,#34026);
#27958=AXIS2_PLACEMENT_3D('',#64062,#34027,#34028);
#27959=AXIS2_PLACEMENT_3D('',#64064,#34029,#34030);
#27960=AXIS2_PLACEMENT_3D('',#64066,#34031,#34032);
#27961=AXIS2_PLACEMENT_3D('',#64067,#34033,#34034);
#27962=AXIS2_PLACEMENT_3D('',#64070,#34036,#34037);
#27963=AXIS2_PLACEMENT_3D('',#64071,#34038,#34039);
#27964=AXIS2_PLACEMENT_3D('',#64073,#34040,#34041);
#27965=AXIS2_PLACEMENT_3D('',#64074,#34042,#34043);
#27966=AXIS2_PLACEMENT_3D('',#64075,#34044,#34045);
#27967=AXIS2_PLACEMENT_3D('',#64088,#34052,#34053);
#27968=AXIS2_PLACEMENT_3D('',#64101,#34060,#34061);
#27969=AXIS2_PLACEMENT_3D('',#64104,#34064,#34065);
#27970=AXIS2_PLACEMENT_3D('',#64106,#34067,#34068);
#27971=AXIS2_PLACEMENT_3D('',#64108,#34070,#34071);
#27972=AXIS2_PLACEMENT_3D('',#64110,#34073,#34074);
#27973=AXIS2_PLACEMENT_3D('',#64112,#34076,#34077);
#27974=AXIS2_PLACEMENT_3D('',#64113,#34078,#34079);
#27975=AXIS2_PLACEMENT_3D('',#64115,#34080,#34081);
#27976=AXIS2_PLACEMENT_3D('',#64116,#34082,#34083);
#27977=AXIS2_PLACEMENT_3D('',#64118,#34084,#34085);
#27978=AXIS2_PLACEMENT_3D('',#64120,#34087,#34088);
#34025=DIRECTION('axis',(0.,0.,1.));
#34026=DIRECTION('refdir',(1.,0.,0.));
#34027=DIRECTION('center_axis',(0.,-1.,0.));
#34028=DIRECTION('ref_axis',(0.,0.,-1.));
#34029=DIRECTION('center_axis',(0.,-1.,0.));
#34030=DIRECTION('ref_axis',(1.,0.,0.));
#34031=DIRECTION('center_axis',(0.,1.,0.));
#34032=DIRECTION('ref_axis',(1.,0.,0.));
#34033=DIRECTION('center_axis',(0.,-1.,0.));
#34034=DIRECTION('ref_axis',(1.,0.,0.));
#34035=DIRECTION('',(0.,1.,0.));
#34036=DIRECTION('center_axis',(0.,-1.,0.));
#34037=DIRECTION('ref_axis',(1.,0.,0.));
#34038=DIRECTION('center_axis',(0.,-1.,0.));
#34039=DIRECTION('ref_axis',(1.,0.,0.));
#34040=DIRECTION('center_axis',(0.,0.,-1.));
#34041=DIRECTION('ref_axis',(-1.,0.,0.));
#34042=DIRECTION('center_axis',(0.,-1.,0.));
#34043=DIRECTION('ref_axis',(1.,0.,0.));
#34044=DIRECTION('center_axis',(2.27272746077357E-11,1.,0.));
#34045=DIRECTION('ref_axis',(1.,-2.27272746077357E-11,0.));
#34046=DIRECTION('',(0.,0.,-1.));
#34047=DIRECTION('',(0.866025403795548,-1.96823971693366E-11,-0.499999999980758));
#34048=DIRECTION('',(0.866025403795548,-1.96823971693366E-11,0.499999999980758));
#34049=DIRECTION('',(0.,0.,1.));
#34050=DIRECTION('',(-0.866025403795548,1.96823971693366E-11,0.499999999980758));
#34051=DIRECTION('',(-0.866025403795548,1.96823971693366E-11,-0.499999999980758));
#34052=DIRECTION('center_axis',(0.,-1.,0.));
#34053=DIRECTION('ref_axis',(0.,0.,-1.));
#34054=DIRECTION('',(0.,0.,1.));
#34055=DIRECTION('',(0.866025403795548,0.,0.499999999980758));
#34056=DIRECTION('',(0.866025403795548,0.,-0.499999999980758));
#34057=DIRECTION('',(0.,0.,-1.));
#34058=DIRECTION('',(-0.866025403795548,0.,-0.499999999980758));
#34059=DIRECTION('',(-0.866025403795548,0.,0.499999999980758));
#34060=DIRECTION('center_axis',(-0.499999999980758,0.,-0.866025403795548));
#34061=DIRECTION('ref_axis',(-0.866025403795548,0.,0.499999999980758));
#34062=DIRECTION('',(0.,-1.,0.));
#34063=DIRECTION('',(0.,-1.,0.));
#34064=DIRECTION('center_axis',(0.499999999980758,0.,-0.866025403795548));
#34065=DIRECTION('ref_axis',(0.,-1.,0.));
#34066=DIRECTION('',(0.,-1.,0.));
#34067=DIRECTION('center_axis',(1.,0.,0.));
#34068=DIRECTION('ref_axis',(0.,1.,0.));
#34069=DIRECTION('',(0.,-1.,0.));
#34070=DIRECTION('center_axis',(0.499999999980758,0.,0.866025403795548));
#34071=DIRECTION('ref_axis',(0.,-1.,0.));
#34072=DIRECTION('',(0.,-1.,0.));
#34073=DIRECTION('center_axis',(-0.499999999980758,0.,0.866025403795548));
#34074=DIRECTION('ref_axis',(0.,1.,0.));
#34075=DIRECTION('',(0.,-1.,0.));
#34076=DIRECTION('center_axis',(-1.,0.,0.));
#34077=DIRECTION('ref_axis',(0.,0.,1.));
#34078=DIRECTION('center_axis',(0.,-1.,0.));
#34079=DIRECTION('ref_axis',(0.,0.,-1.));
#34080=DIRECTION('center_axis',(0.,-1.,0.));
#34081=DIRECTION('ref_axis',(1.,0.,0.));
#34082=DIRECTION('center_axis',(0.,1.,0.));
#34083=DIRECTION('ref_axis',(1.,0.,0.));
#34084=DIRECTION('center_axis',(0.,-1.,0.));
#34085=DIRECTION('ref_axis',(1.,0.,0.));
#34086=DIRECTION('',(0.707106781186547,-0.707106781186548,-8.65956056235493E-17));
#34087=DIRECTION('center_axis',(0.,-1.,0.));
#34088=DIRECTION('ref_axis',(1.,0.,0.));
#34089=DIRECTION('',(0.,1.,0.));
#64061=CARTESIAN_POINT('',(0.,0.,0.));
#64062=CARTESIAN_POINT('Origin',(26.5,12.,20.));
#64063=CARTESIAN_POINT('',(19.,12.,20.));
#64064=CARTESIAN_POINT('Origin',(24.,12.,20.));
#64065=CARTESIAN_POINT('',(21.,12.,20.));
#64066=CARTESIAN_POINT('Origin',(24.,12.,20.));
#64067=CARTESIAN_POINT('Origin',(24.,14.7,20.));
#64068=CARTESIAN_POINT('',(19.,17.4,20.));
#64069=CARTESIAN_POINT('',(19.,14.7,20.));
#64070=CARTESIAN_POINT('Origin',(24.,17.4,20.));
#64071=CARTESIAN_POINT('Origin',(24.,17.3999999999,20.));
#64072=CARTESIAN_POINT('',(19.6,17.9999999999,20.));
#64073=CARTESIAN_POINT('Origin',(19.6000000001,17.3999999999,20.));
#64074=CARTESIAN_POINT('Origin',(24.,17.9999999999,20.));
#64075=CARTESIAN_POINT('Origin',(26.2,17.99999999995,20.));
#64076=CARTESIAN_POINT('',(21.5,18.,21.443375673));
#64077=CARTESIAN_POINT('',(21.5,18.,18.556624327));
#64078=CARTESIAN_POINT('',(21.5,18.,20.));
#64079=CARTESIAN_POINT('',(24.,18.,17.1132486541));
#64080=CARTESIAN_POINT('',(23.5750000000476,18.,17.3586225184655));
#64081=CARTESIAN_POINT('',(26.5,18.,18.556624327));
#64082=CARTESIAN_POINT('',(26.0749999999947,18.,18.3112504626039));
#64083=CARTESIAN_POINT('',(26.5,18.,21.443375673));
#64084=CARTESIAN_POINT('',(26.5,18.,19.63915608175));
#64085=CARTESIAN_POINT('',(24.,18.,22.8867513459));
#64086=CARTESIAN_POINT('',(26.0749999999947,18.,21.6887495373961));
#64087=CARTESIAN_POINT('',(23.5750000000476,18.,22.6413774815345));
#64088=CARTESIAN_POINT('Origin',(24.,15.,20.));
#64089=CARTESIAN_POINT('',(21.5,15.,18.556624327));
#64090=CARTESIAN_POINT('',(21.5,15.,21.443375673));
#64091=CARTESIAN_POINT('',(21.5,15.,21.443375673));
#64092=CARTESIAN_POINT('',(24.,15.,22.8867513459));
#64093=CARTESIAN_POINT('',(24.,15.,22.8867513459));
#64094=CARTESIAN_POINT('',(26.5,15.,21.443375673));
#64095=CARTESIAN_POINT('',(26.5,15.,21.443375673));
#64096=CARTESIAN_POINT('',(26.5,15.,18.556624327));
#64097=CARTESIAN_POINT('',(26.5,15.,20.));
#64098=CARTESIAN_POINT('',(24.,15.,17.1132486541));
#64099=CARTESIAN_POINT('',(24.,15.,17.1132486541));
#64100=CARTESIAN_POINT('',(21.5,15.,18.556624327));
#64101=CARTESIAN_POINT('Origin',(22.75,18.,17.83493649055));
#64102=CARTESIAN_POINT('',(24.,18.,17.1132486541));
#64103=CARTESIAN_POINT('',(21.5,18.,18.556624327));
#64104=CARTESIAN_POINT('Origin',(25.25,18.,17.83493649055));
#64105=CARTESIAN_POINT('',(26.5,18.,18.556624327));
#64106=CARTESIAN_POINT('Origin',(26.5,18.,19.2783121635));
#64107=CARTESIAN_POINT('',(26.5,18.,21.443375673));
#64108=CARTESIAN_POINT('Origin',(25.25,18.,22.16506350945));
#64109=CARTESIAN_POINT('',(24.,18.,22.8867513459));
#64110=CARTESIAN_POINT('Origin',(22.75,18.,22.16506350945));
#64111=CARTESIAN_POINT('',(21.5,18.,21.443375673));
#64112=CARTESIAN_POINT('Origin',(21.5,18.,20.));
#64113=CARTESIAN_POINT('Origin',(25.193275,-8.,20.));
#64114=CARTESIAN_POINT('',(21.61345,-8.,20.));
#64115=CARTESIAN_POINT('Origin',(24.,-8.,20.));
#64116=CARTESIAN_POINT('Origin',(24.,-7.693275,20.));
#64117=CARTESIAN_POINT('',(21.,-7.38655,20.));
#64118=CARTESIAN_POINT('Origin',(24.,-7.38655,20.));
#64119=CARTESIAN_POINT('',(21.306725,-7.693275,20.));
#64120=CARTESIAN_POINT('Origin',(24.,2.306725,20.));
#64121=CARTESIAN_POINT('',(21.,2.306725,20.));
#66668=UNCERTAINTY_MEASURE_WITH_UNIT(LENGTH_MEASURE(0.01),#66722,
'DISTANCE_ACCURACY_VALUE',
'Maximum model space distance between geometric entities at asserted c
onnectivities');
#66680=UNCERTAINTY_MEASURE_WITH_UNIT(LENGTH_MEASURE(0.01),#66722,
'DISTANCE_ACCURACY_VALUE',
'Maximum model space distance between geometric entities at asserted c
onnectivities');
#66709=(
GEOMETRIC_REPRESENTATION_CONTEXT(3)
GLOBAL_UNCERTAINTY_ASSIGNED_CONTEXT((#66668))
GLOBAL_UNIT_ASSIGNED_CONTEXT((#66722,#66724,#66725))
REPRESENTATION_CONTEXT('','3D')
);
#66721=(
GEOMETRIC_REPRESENTATION_CONTEXT(3)
GLOBAL_UNCERTAINTY_ASSIGNED_CONTEXT((#66680))
GLOBAL_UNIT_ASSIGNED_CONTEXT((#66722,#66724,#66725))
REPRESENTATION_CONTEXT('','3D')
);
#66722=(
LENGTH_UNIT()
NAMED_UNIT(*)
SI_UNIT(.MILLI.,.METRE.)
);
#66724=(
NAMED_UNIT(*)
PLANE_ANGLE_UNIT()
SI_UNIT($,.RADIAN.)
);
#66725=(
NAMED_UNIT(*)
SI_UNIT($,.STERADIAN.)
SOLID_ANGLE_UNIT()
);
#66754=SHAPE_DEFINITION_REPRESENTATION(#66814,#66918);
#66814=PRODUCT_DEFINITION_SHAPE('',$,#66959);
#66918=SHAPE_REPRESENTATION('',(#27957),#66709);
#66930=PRODUCT_DEFINITION_CONTEXT('part definition',#67052,'design');
#66959=PRODUCT_DEFINITION('Coupling Clamp Screw 1',
'Coupling Clamp Screw 1',#66999,#66930);
#66999=PRODUCT_DEFINITION_FORMATION('',$,#67082);
#67052=APPLICATION_CONTEXT(
'Core Data for Automotive Mechanical Design Process');
#67053=PRODUCT_CONTEXT('part definition',#67052,'mechanical');
#67082=PRODUCT('Coupling Clamp Screw 1','Coupling Clamp Screw 1',$,(#67053));
#67095=PRESENTATION_STYLE_ASSIGNMENT((#67097));
#67097=SURFACE_STYLE_USAGE(.BOTH.,#67099);
#67099=SURFACE_SIDE_STYLE('',(#67101));
#67101=SURFACE_STYLE_FILL_AREA(#67103);
#67103=FILL_AREA_STYLE('Opaque(202,209,238)',(#67105));
#67105=FILL_AREA_STYLE_COLOUR('Opaque(202,209,238)',#67107);
#67107=COLOUR_RGB('Opaque(202,209,238)',0.792156862745098,0.819607843137255,
0.933333333333333);
ENDSEC;
END-ISO-10303-21;
